ISO-10303-21;
HEADER;
/* Generated by software containing ST-Developer
 * from STEP Tools, Inc. (www.steptools.com) 
 */

FILE_DESCRIPTION(
/* description */ (''),
/* implementation_level */ '2;1');

FILE_NAME(
/* name */ '06_Backup_Ring_30x2_PTFE.step',
/* time_stamp */ '2026-10-26T03:55:20-07:00',
/* author */ (''),
/* organization */ (''),
/* preprocessor_version */ 'ST-DEVELOPER v20.2',
/* originating_system */ 'Autodesk Translation Framework v15.15.0.0',
/* authorisation */ '');

FILE_SCHEMA (('AUTOMOTIVE_DESIGN { 1 0 10303 214 3 1 1 }'));
ENDSEC;

DATA;
#10=MECHANICAL_DESIGN_GEOMETRIC_PRESENTATION_REPRESENTATION('',(#180),#45236);
#140=SHAPE_REPRESENTATION_RELATIONSHIP('SRR','None',#45319,#160);
#160=ADVANCED_BREP_SHAPE_REPRESENTATION('',(#200),#45221);
#180=STYLED_ITEM('',(#45498),#200);
#200=MANIFOLD_SOLID_BREP('Body1',#16522);
#963=FACE_BOUND('',#3092,.T.);
#964=FACE_BOUND('',#3095,.T.);
#1132=PLANE('',#17160);
#1133=PLANE('',#17164);
#1681=CYLINDRICAL_SURFACE('',#17157,15.06);
#1682=CYLINDRICAL_SURFACE('',#17162,17.97);
#2092=FACE_OUTER_BOUND('',#3090,.T.);
#2093=FACE_OUTER_BOUND('',#3091,.T.);
#2094=FACE_OUTER_BOUND('',#3093,.T.);
#2095=FACE_OUTER_BOUND('',#3094,.T.);
#3090=EDGE_LOOP('',(#12138,#12139,#12140,#12141));
#3091=EDGE_LOOP('',(#12142));
#3092=EDGE_LOOP('',(#12143));
#3093=EDGE_LOOP('',(#12144,#12145,#12146,#12147));
#3094=EDGE_LOOP('',(#12148));
#3095=EDGE_LOOP('',(#12149));
#4166=LINE('',#32237,#5477);
#4167=LINE('',#32245,#5478);
#5477=VECTOR('',#19205,15.06);
#5478=VECTOR('',#19216,17.97);
#6665=CIRCLE('',#17158,15.06);
#6666=CIRCLE('',#17159,15.06);
#6667=CIRCLE('',#17161,17.97);
#6668=CIRCLE('',#17163,17.97);
#7380=VERTEX_POINT('',#32234);
#7381=VERTEX_POINT('',#32236);
#7382=VERTEX_POINT('',#32240);
#7383=VERTEX_POINT('',#32243);
#9132=EDGE_CURVE('',#7380,#7380,#6665,.T.);
#9133=EDGE_CURVE('',#7380,#7381,#4166,.T.);
#9134=EDGE_CURVE('',#7381,#7381,#6666,.T.);
#9135=EDGE_CURVE('',#7382,#7382,#6667,.T.);
#9136=EDGE_CURVE('',#7383,#7383,#6668,.T.);
#9137=EDGE_CURVE('',#7383,#7382,#4167,.T.);
#12138=ORIENTED_EDGE('',*,*,#9132,.T.);
#12139=ORIENTED_EDGE('',*,*,#9133,.T.);
#12140=ORIENTED_EDGE('',*,*,#9134,.F.);
#12141=ORIENTED_EDGE('',*,*,#9133,.F.);
#12142=ORIENTED_EDGE('',*,*,#9135,.F.);
#12143=ORIENTED_EDGE('',*,*,#9134,.T.);
#12144=ORIENTED_EDGE('',*,*,#9136,.F.);
#12145=ORIENTED_EDGE('',*,*,#9137,.T.);
#12146=ORIENTED_EDGE('',*,*,#9135,.T.);
#12147=ORIENTED_EDGE('',*,*,#9137,.F.);
#12148=ORIENTED_EDGE('',*,*,#9136,.T.);
#12149=ORIENTED_EDGE('',*,*,#9132,.F.);
#15820=ADVANCED_FACE('',(#2092),#1681,.F.);
#15821=ADVANCED_FACE('',(#2093,#963),#1132,.T.);
#15822=ADVANCED_FACE('',(#2094),#1682,.T.);
#15823=ADVANCED_FACE('',(#2095,#964),#1133,.T.);
#16522=CLOSED_SHELL('',(#15820,#15821,#15822,#15823));
#17156=AXIS2_PLACEMENT_3D('',#32232,#19199,#19200);
#17157=AXIS2_PLACEMENT_3D('',#32233,#19201,#19202);
#17158=AXIS2_PLACEMENT_3D('',#32235,#19203,#19204);
#17159=AXIS2_PLACEMENT_3D('',#32238,#19206,#19207);
#17160=AXIS2_PLACEMENT_3D('',#32239,#19208,#19209);
#17161=AXIS2_PLACEMENT_3D('',#32241,#19210,#19211);
#17162=AXIS2_PLACEMENT_3D('',#32242,#19212,#19213);
#17163=AXIS2_PLACEMENT_3D('',#32244,#19214,#19215);
#17164=AXIS2_PLACEMENT_3D('',#32246,#19217,#19218);
#19199=DIRECTION('axis',(0.,0.,1.));
#19200=DIRECTION('refdir',(1.,0.,0.));
#19201=DIRECTION('center_axis',(1.,0.,0.));
#19202=DIRECTION('ref_axis',(0.,1.,0.));
#19203=DIRECTION('center_axis',(1.,0.,0.));
#19204=DIRECTION('ref_axis',(0.,0.,-1.));
#19205=DIRECTION('',(-1.,0.,0.));
#19206=DIRECTION('center_axis',(1.,0.,0.));
#19207=DIRECTION('ref_axis',(0.,0.,-1.));
#19208=DIRECTION('center_axis',(-1.,0.,0.));
#19209=DIRECTION('ref_axis',(0.,0.,1.));
#19210=DIRECTION('center_axis',(1.,0.,0.));
#19211=DIRECTION('ref_axis',(0.,0.,-1.));
#19212=DIRECTION('center_axis',(1.,0.,0.));
#19213=DIRECTION('ref_axis',(0.,1.,0.));
#19214=DIRECTION('center_axis',(1.,0.,0.));
#19215=DIRECTION('ref_axis',(0.,0.,-1.));
#19216=DIRECTION('',(-1.,0.,0.));
#19217=DIRECTION('center_axis',(1.,0.,0.));
#19218=DIRECTION('ref_axis',(0.,0.,-1.));
#32232=CARTESIAN_POINT('',(0.,0.,0.));
#32233=CARTESIAN_POINT('Origin',(0.99,0.,0.));
#32234=CARTESIAN_POINT('',(1.98,-15.06,-1.84431807951591E-15));
#32235=CARTESIAN_POINT('Origin',(1.98,0.,0.));
#32236=CARTESIAN_POINT('',(1.38777878078145E-16,-15.06,-1.84431807951591E-15));
#32237=CARTESIAN_POINT('',(0.99,-15.06,-1.84431807951591E-15));
#32238=CARTESIAN_POINT('Origin',(0.,0.,0.));
#32239=CARTESIAN_POINT('Origin',(0.,17.97,0.));
#32240=CARTESIAN_POINT('',(0.,-17.97,-2.20069029806779E-15));
#32241=CARTESIAN_POINT('Origin',(0.,0.,0.));
#32242=CARTESIAN_POINT('Origin',(0.99,0.,0.));
#32243=CARTESIAN_POINT('',(1.98,-17.97,-2.20069029806779E-15));
#32244=CARTESIAN_POINT('Origin',(1.98,0.,0.));
#32245=CARTESIAN_POINT('',(0.99,-17.97,-2.20069029806779E-15));
#32246=CARTESIAN_POINT('Origin',(1.98,15.06,0.));
#45199=UNCERTAINTY_MEASURE_WITH_UNIT(LENGTH_MEASURE(0.01),#45237,
'DISTANCE_ACCURACY_VALUE',
'Maximum model space distance between geometric entities at asserted c
onnectivities');
#45214=UNCERTAINTY_MEASURE_WITH_UNIT(LENGTH_MEASURE(0.01),#45237,
'DISTANCE_ACCURACY_VALUE',
'Maximum model space distance between geometric entities at asserted c
onnectivities');
#45221=(
GEOMETRIC_REPRESENTATION_CONTEXT(3)
GLOBAL_UNCERTAINTY_ASSIGNED_CONTEXT((#45199))
GLOBAL_UNIT_ASSIGNED_CONTEXT((#45237,#45239,#45240))
REPRESENTATION_CONTEXT('','3D')
);
#45236=(
GEOMETRIC_REPRESENTATION_CONTEXT(3)
GLOBAL_UNCERTAINTY_ASSIGNED_CONTEXT((#45214))
GLOBAL_UNIT_ASSIGNED_CONTEXT((#45237,#45239,#45240))
REPRESENTATION_CONTEXT('','3D')
);
#45237=(
LENGTH_UNIT()
NAMED_UNIT(*)
SI_UNIT(.MILLI.,.METRE.)
);
#45239=(
NAMED_UNIT(*)
PLANE_ANGLE_UNIT()
SI_UNIT($,.RADIAN.)
);
#45240=(
NAMED_UNIT(*)
SI_UNIT($,.STERADIAN.)
SOLID_ANGLE_UNIT()
);
#45247=SHAPE_DEFINITION_REPRESENTATION(#45268,#45319);
#45268=PRODUCT_DEFINITION_SHAPE('',$,#45341);
#45319=SHAPE_REPRESENTATION('',(#17156),#45221);
#45334=PRODUCT_DEFINITION_CONTEXT('part definition',#45399,'design');
#45341=PRODUCT_DEFINITION('2026-10-25-23-38-17-064',
'06_Backup_Ring_30x2_PTFE',#45362,#45334);
#45362=PRODUCT_DEFINITION_FORMATION('',$,#45407);
#45399=APPLICATION_CONTEXT(
'Core Data for Automotive Mechanical Design Process');
#45400=PRODUCT_CONTEXT('part definition',#45399,'mechanical');
#45407=PRODUCT('2026-10-25-23-38-17-064','06_Backup_Ring_30x2_PTFE',$,(#45400));
#45492=COLOUR_RGB('Off White',0.89,0.88,0.83);
#45493=FILL_AREA_STYLE_COLOUR('',#45492);
#45494=FILL_AREA_STYLE('',(#45493));
#45495=SURFACE_STYLE_FILL_AREA(#45494);
#45496=SURFACE_SIDE_STYLE('',(#45495));
#45497=SURFACE_STYLE_USAGE(.BOTH.,#45496);
#45498=PRESENTATION_STYLE_ASSIGNMENT((#45497));
ENDSEC;
END-ISO-10303-21;
